ISO-10303-21;
HEADER;
FILE_DESCRIPTION (('STEP AP214'),
    '1' );
FILE_NAME ('Ball Separator Polymer.step',
    '2026-10-09T12:49:55',
    ( '' ),
    ( '' ),
    'SwSTEP 2.0',
    'SolidWorks 2026',
    '' );
FILE_SCHEMA (( 'AUTOMOTIVE_DESIGN' ));
ENDSEC;

DATA;
#32=STYLED_ITEM ( 'NONE', ( #1106 ), #1548 ) ;
#114=FILL_AREA_STYLE_COLOUR ( '', #3598 ) ;
#191=CIRCLE ( 'NONE', #10174, 8.000000000000007105 ) ;
#313=( LENGTH_UNIT ( ) NAMED_UNIT ( * ) SI_UNIT ( .MILLI., .METRE. ) );
#436=EDGE_LOOP ( 'NONE', ( #2663, #922, #6967, #12561 ) ) ;
#496=ADVANCED_FACE ( 'NONE', ( #4803 ), #9936, .T. ) ;
#515=DIRECTION ( 'NONE',  ( -1.000000000000000000, 0.000000000000000000, 0.000000000000000000 ) ) ;
#707=( LENGTH_UNIT ( ) NAMED_UNIT ( * ) SI_UNIT ( .MILLI., .METRE. ) );
#805=AXIS2_PLACEMENT_3D ( 'NONE', #6711, #10765, #10635 ) ;
#810=DIRECTION ( 'NONE',  ( -1.000000000000000000, 0.000000000000000000, 0.000000000000000000 ) ) ;
#922=ORIENTED_EDGE ( 'NONE', *, *, #9814, .T. ) ;
#1106=PRESENTATION_STYLE_ASSIGNMENT (( #4169 ) ) ;
#1140=AXIS2_PLACEMENT_3D ( 'NONE', #3870, #810, #11684 ) ;
#1176=( NAMED_UNIT ( * ) PLANE_ANGLE_UNIT ( ) SI_UNIT ( $, .RADIAN. ) );
#1329=EDGE_CURVE ( 'NONE', #2886, #5106, #6001, .T. ) ;
#1393=PRODUCT ( 'Ball Separator Polymer', 'Ball Separator Polymer', '', ( #5394 ) ) ;
#1449=DIRECTION ( 'NONE',  ( 0.000000000000000000, 0.000000000000000000, 1.000000000000000000 ) ) ;
#1548=MANIFOLD_SOLID_BREP ( 'NONE', #2405 ) ;
#1849=CYLINDRICAL_SURFACE ( 'NONE', #8470, 8.000000000000007105 ) ;
#1972=AXIS2_PLACEMENT_3D ( 'NONE', #12144, #3126, #4939 ) ;
#2098=( NAMED_UNIT ( * ) SI_UNIT ( $, .STERADIAN. ) SOLID_ANGLE_UNIT ( ) );
#2169=FILL_AREA_STYLE ('',( #114 ) ) ;
#2279=PRODUCT_DEFINITION_CONTEXT ( 'detailed design', #6854, 'design' ) ;
#2327=MECHANICAL_DESIGN_GEOMETRIC_PRESENTATION_REPRESENTATION('',(#32),#8930);
#2345=PRODUCT_DEFINITION_SHAPE ( 'NONE', 'NONE',  #10447 ) ;
#2405=CLOSED_SHELL ( 'NONE', ( #12989, #496, #11197, #7786 ) ) ;
#2565=LINE ( 'NONE', #5444, #9447 ) ;
#2572=DIRECTION ( 'NONE',  ( 0.000000000000000000, 0.000000000000000000, 1.000000000000000000 ) ) ;
#2636=CARTESIAN_POINT ( 'NONE',  ( 0.000000000000000000, 0.000000000000000000, 250.0000000000000000 ) ) ;
#2663=ORIENTED_EDGE ( 'NONE', *, *, #11525, .T. ) ;
#2886=VERTEX_POINT ( 'NONE', #7372 ) ;
#3126=DIRECTION ( 'NONE',  ( -1.000000000000000000, 0.000000000000000000, 0.000000000000000000 ) ) ;
#3371=DIRECTION ( 'NONE',  ( -1.000000000000000000, 0.000000000000000000, 0.000000000000000000 ) ) ;
#3416=ORIENTED_EDGE ( 'NONE', *, *, #7386, .T. ) ;
#3442=VECTOR ( 'NONE', #10505, 1000.000000000000000 ) ;
#3444=SHAPE_DEFINITION_REPRESENTATION ( #2345, #5191 ) ;
#3484=SPHERICAL_SURFACE ( 'NONE', #11590, 10.00000000000000000 ) ;
#3598=COLOUR_RGB ( '', 0.31764706, 0.68627451, 0.89019608) ;
#3669=ORIENTED_EDGE ( 'NONE', *, *, #5588, .F. ) ;
#3710=DIRECTION ( 'NONE',  ( -1.000000000000000000, 0.000000000000000000, 0.000000000000000000 ) ) ;
#3870=CARTESIAN_POINT ( 'NONE',  ( 0.000000000000000000, 0.000000000000000000, 250.0000000000000000 ) ) ;
#3923=DIRECTION ( 'NONE',  ( 0.000000000000000000, -1.000000000000000000, 0.000000000000000000 ) ) ;
#4132=EDGE_LOOP ( 'NONE', ( #11800, #11969 ) ) ;
#4169=SURFACE_STYLE_USAGE ( .BOTH. , #11436 ) ;
#4451=ORIENTED_EDGE ( 'NONE', *, *, #5588, .T. ) ;
#4480=FACE_OUTER_BOUND ( 'NONE', #4848, .T. ) ;
#4536=DIRECTION ( 'NONE',  ( 0.000000000000000000, 0.000000000000000000, 1.000000000000000000 ) ) ;
#4786=CARTESIAN_POINT ( 'NONE',  ( 11.00000000000000000, 0.000000000000000000, 250.0000000000000000 ) ) ;
#4803=FACE_OUTER_BOUND ( 'NONE', #10689, .T. ) ;
#4848=EDGE_LOOP ( 'NONE', ( #6896, #4451 ) ) ;
#4939=DIRECTION ( 'NONE',  ( 0.000000000000000000, 0.000000000000000000, 1.000000000000000000 ) ) ;
#5106=VERTEX_POINT ( 'NONE', #10087 ) ;
#5112=ORIENTED_EDGE ( 'NONE', *, *, #9814, .F. ) ;
#5191=SHAPE_REPRESENTATION ( 'Ball Separator Polymer', ( #805 ), #9955 ) ;
#5394=PRODUCT_CONTEXT ( 'NONE', #5679, 'mechanical' ) ;
#5431=DIRECTION ( 'NONE',  ( 0.000000000000000000, 1.000000000000000000, 0.000000000000000000 ) ) ;
#5444=CARTESIAN_POINT ( 'NONE',  ( 0.000000000000000000, 0.000000000000000000, 258.0000000000000000 ) ) ;
#5588=EDGE_CURVE ( 'NONE', #5106, #2886, #191, .T. ) ;
#5663=DIRECTION ( 'NONE',  ( 1.000000000000000000, 0.000000000000000000, -0.000000000000000000 ) ) ;
#5679=APPLICATION_CONTEXT ( 'automotive_design' ) ;
#5691=VERTEX_POINT ( 'NONE', #9073 ) ;
#6001=CIRCLE ( 'NONE', #6206, 8.000000000000007105 ) ;
#6206=AXIS2_PLACEMENT_3D ( 'NONE', #11653, #3710, #2572 ) ;
#6320=ORIENTED_EDGE ( 'NONE', *, *, #10030, .T. ) ;
#6369=AXIS2_PLACEMENT_3D ( 'NONE', #4786, #5663, #3923 ) ;
#6444=CARTESIAN_POINT ( 'NONE',  ( 0.000000000000000000, 9.797174393178825657E-16, 242.0000000000000000 ) ) ;
#6711=CARTESIAN_POINT ( 'NONE',  ( 0.000000000000000000, 0.000000000000000000, 0.000000000000000000 ) ) ;
#6833=PRODUCT_DEFINITION_FORMATION_WITH_SPECIFIED_SOURCE ( 'ANY', '', #1393, .NOT_KNOWN. ) ;
#6854=APPLICATION_CONTEXT ( 'automotive_design' ) ;
#6896=ORIENTED_EDGE ( 'NONE', *, *, #1329, .T. ) ;
#6919=FACE_OUTER_BOUND ( 'NONE', #436, .T. ) ;
#6967=ORIENTED_EDGE ( 'NONE', *, *, #1329, .F. ) ;
#6977=DIRECTION ( 'NONE',  ( 0.000000000000000000, 0.000000000000000000, 1.000000000000000000 ) ) ;
#7372=CARTESIAN_POINT ( 'NONE',  ( -5.000000000000000000, 0.000000000000000000, 258.0000000000000000 ) ) ;
#7386=EDGE_CURVE ( 'NONE', #10752, #2886, #2565, .T. ) ;
#7504=CIRCLE ( 'NONE', #1972, 8.000000000000007105 ) ;
#7617=CARTESIAN_POINT ( 'NONE',  ( 5.000000000000000000, 0.000000000000000000, 258.0000000000000000 ) ) ;
#7786=ADVANCED_FACE ( 'NONE', ( #4480 ), #3484, .F. ) ;
#8397=CARTESIAN_POINT ( 'NONE',  ( 5.000000000000000000, 0.000000000000000000, 250.0000000000000000 ) ) ;
#8428=UNCERTAINTY_MEASURE_WITH_UNIT (LENGTH_MEASURE( 1.000000000000000082E-05 ), #707, 'distance_accuracy_value', 'NONE');
#8470=AXIS2_PLACEMENT_3D ( 'NONE', #2636, #8713, #6977 ) ;
#8713=DIRECTION ( 'NONE',  ( -1.000000000000000000, 0.000000000000000000, 0.000000000000000000 ) ) ;
#8930=( GEOMETRIC_REPRESENTATION_CONTEXT ( 3 ) GLOBAL_UNCERTAINTY_ASSIGNED_CONTEXT ( ( #12169 ) ) GLOBAL_UNIT_ASSIGNED_CONTEXT ( ( #313, #1176, #2098 ) ) REPRESENTATION_CONTEXT ( 'NONE', 'WORKASPACE' ) );
#8931=SPHERICAL_SURFACE ( 'NONE', #6369, 10.00000000000000000 ) ;
#9073=CARTESIAN_POINT ( 'NONE',  ( 5.000000000000000000, 9.797174393178815797E-16, 242.0000000000000000 ) ) ;
#9240=SURFACE_STYLE_FILL_AREA ( #2169 ) ;
#9343=CIRCLE ( 'NONE', #11689, 8.000000000000007105 ) ;
#9447=VECTOR ( 'NONE', #515, 1000.000000000000000 ) ;
#9623=LINE ( 'NONE', #6444, #3442 ) ;
#9729=DIRECTION ( 'NONE',  ( -1.000000000000000000, 0.000000000000000000, 0.000000000000000000 ) ) ;
#9814=EDGE_CURVE ( 'NONE', #5691, #5106, #9623, .T. ) ;
#9936=CYLINDRICAL_SURFACE ( 'NONE', #1140, 8.000000000000007105 ) ;
#9955=( GEOMETRIC_REPRESENTATION_CONTEXT ( 3 ) GLOBAL_UNCERTAINTY_ASSIGNED_CONTEXT ( ( #8428 ) ) GLOBAL_UNIT_ASSIGNED_CONTEXT ( ( #707, #9959, #13027 ) ) REPRESENTATION_CONTEXT ( 'NONE', 'WORKASPACE' ) );
#9959=( NAMED_UNIT ( * ) PLANE_ANGLE_UNIT ( ) SI_UNIT ( $, .RADIAN. ) );
#10027=SHAPE_REPRESENTATION_RELATIONSHIP ( 'NONE' , 'NONE' ,  #5191, #13034 ) ;
#10030=EDGE_CURVE ( 'NONE', #5691, #10752, #7504, .T. ) ;
#10087=CARTESIAN_POINT ( 'NONE',  ( -5.000000000000000000, 9.797174393178815797E-16, 242.0000000000000000 ) ) ;
#10174=AXIS2_PLACEMENT_3D ( 'NONE', #12806, #9729, #4536 ) ;
#10447=PRODUCT_DEFINITION ( 'UNKNOWN', '', #6833, #2279 ) ;
#10505=DIRECTION ( 'NONE',  ( -1.000000000000000000, 0.000000000000000000, 0.000000000000000000 ) ) ;
#10635=DIRECTION ( 'NONE',  ( 1.000000000000000000, 0.000000000000000000, 0.000000000000000000 ) ) ;
#10689=EDGE_LOOP ( 'NONE', ( #5112, #6320, #3416, #3669 ) ) ;
#10752=VERTEX_POINT ( 'NONE', #7617 ) ;
#10765=DIRECTION ( 'NONE',  ( 0.000000000000000000, 0.000000000000000000, 1.000000000000000000 ) ) ;
#10790=FACE_OUTER_BOUND ( 'NONE', #4132, .T. ) ;
#11197=ADVANCED_FACE ( 'NONE', ( #10790 ), #8931, .F. ) ;
#11436=SURFACE_SIDE_STYLE ('',( #9240 ) ) ;
#11525=EDGE_CURVE ( 'NONE', #10752, #5691, #9343, .T. ) ;
#11590=AXIS2_PLACEMENT_3D ( 'NONE', #12558, #11698, #5431 ) ;
#11653=CARTESIAN_POINT ( 'NONE',  ( -5.000000000000000000, 0.000000000000000000, 250.0000000000000000 ) ) ;
#11684=DIRECTION ( 'NONE',  ( 0.000000000000000000, 0.000000000000000000, 1.000000000000000000 ) ) ;
#11689=AXIS2_PLACEMENT_3D ( 'NONE', #8397, #3371, #1449 ) ;
#11698=DIRECTION ( 'NONE',  ( 1.000000000000000000, -0.000000000000000000, 0.000000000000000000 ) ) ;
#11800=ORIENTED_EDGE ( 'NONE', *, *, #11525, .F. ) ;
#11969=ORIENTED_EDGE ( 'NONE', *, *, #10030, .F. ) ;
#12144=CARTESIAN_POINT ( 'NONE',  ( 5.000000000000000000, 0.000000000000000000, 250.0000000000000000 ) ) ;
#12169=UNCERTAINTY_MEASURE_WITH_UNIT (LENGTH_MEASURE( 1.000000000000000082E-05 ), #313, 'distance_accuracy_value', 'NONE');
#12558=CARTESIAN_POINT ( 'NONE',  ( -11.00000000000000000, 0.000000000000000000, 250.0000000000000000 ) ) ;
#12561=ORIENTED_EDGE ( 'NONE', *, *, #7386, .F. ) ;
#12806=CARTESIAN_POINT ( 'NONE',  ( -5.000000000000000000, 0.000000000000000000, 250.0000000000000000 ) ) ;
#12989=ADVANCED_FACE ( 'NONE', ( #6919 ), #1849, .T. ) ;
#13027=( NAMED_UNIT ( * ) SI_UNIT ( $, .STERADIAN. ) SOLID_ANGLE_UNIT ( ) );
#13034=ADVANCED_BREP_SHAPE_REPRESENTATION ( '', ( #1548, #805 ), #9955 ) ;
ENDSEC;
END-ISO-10303-21;
